ISO-10303-21;
HEADER;
/* Generated by software containing ST-Developer
 * from STEP Tools, Inc. (www.steptools.com) 
 */

FILE_DESCRIPTION(
/* description */ (''),
/* implementation_level */ '2;1');

FILE_NAME(
/* name */ 'Base.step',
/* time_stamp */ '2026-10-19T02:00:06+06:00',
/* author */ (''),
/* organization */ (''),
/* preprocessor_version */ 'ST-DEVELOPER v20.2',
/* originating_system */ 'Autodesk Translation Framework v15.15.0.0',
/* authorisation */ '');

FILE_SCHEMA (('AUTOMOTIVE_DESIGN { 1 0 10303 214 3 1 1 }'));
ENDSEC;

DATA;
#10=MECHANICAL_DESIGN_GEOMETRIC_PRESENTATION_REPRESENTATION('',(#111),#4833);
#89=SHAPE_REPRESENTATION_RELATIONSHIP('SRR','None',#4880,#100);
#100=ADVANCED_BREP_SHAPE_REPRESENTATION('',(#122),#4828);
#111=STYLED_ITEM('',(#4971),#122);
#122=MANIFOLD_SOLID_BREP('Base',#2693);
#215=PLANE('',#2959);
#216=PLANE('',#2960);
#217=PLANE('',#2961);
#218=PLANE('',#2962);
#219=PLANE('',#2963);
#220=PLANE('',#2964);
#221=PLANE('',#2965);
#222=PLANE('',#2966);
#223=PLANE('',#2967);
#224=PLANE('',#2968);
#225=PLANE('',#2969);
#351=FACE_OUTER_BOUND('',#527,.T.);
#352=FACE_OUTER_BOUND('',#528,.T.);
#353=FACE_OUTER_BOUND('',#529,.T.);
#354=FACE_OUTER_BOUND('',#530,.T.);
#355=FACE_OUTER_BOUND('',#531,.T.);
#356=FACE_OUTER_BOUND('',#532,.T.);
#357=FACE_OUTER_BOUND('',#533,.T.);
#358=FACE_OUTER_BOUND('',#534,.T.);
#359=FACE_OUTER_BOUND('',#535,.T.);
#360=FACE_OUTER_BOUND('',#536,.T.);
#361=FACE_OUTER_BOUND('',#537,.T.);
#527=EDGE_LOOP('',(#2093,#2094,#2095,#2096));
#528=EDGE_LOOP('',(#2097,#2098,#2099,#2100));
#529=EDGE_LOOP('',(#2101,#2102,#2103,#2104));
#530=EDGE_LOOP('',(#2105,#2106,#2107,#2108));
#531=EDGE_LOOP('',(#2109,#2110,#2111,#2112));
#532=EDGE_LOOP('',(#2113,#2114,#2115,#2116));
#533=EDGE_LOOP('',(#2117,#2118,#2119,#2120));
#534=EDGE_LOOP('',(#2121,#2122,#2123,#2124));
#535=EDGE_LOOP('',(#2125,#2126,#2127,#2128));
#536=EDGE_LOOP('',(#2129,#2130,#2131,#2132,#2133,#2134,#2135,#2136,#2137));
#537=EDGE_LOOP('',(#2138,#2139,#2140,#2141,#2142,#2143,#2144,#2145,#2146));
#737=LINE('',#4236,#991);
#738=LINE('',#4238,#992);
#739=LINE('',#4240,#993);
#740=LINE('',#4241,#994);
#741=LINE('',#4244,#995);
#742=LINE('',#4246,#996);
#743=LINE('',#4247,#997);
#744=LINE('',#4250,#998);
#745=LINE('',#4252,#999);
#746=LINE('',#4253,#1000);
#747=LINE('',#4256,#1001);
#748=LINE('',#4258,#1002);
#749=LINE('',#4259,#1003);
#750=LINE('',#4262,#1004);
#751=LINE('',#4264,#1005);
#752=LINE('',#4265,#1006);
#753=LINE('',#4268,#1007);
#754=LINE('',#4270,#1008);
#755=LINE('',#4271,#1009);
#756=LINE('',#4274,#1010);
#757=LINE('',#4276,#1011);
#758=LINE('',#4277,#1012);
#759=LINE('',#4280,#1013);
#760=LINE('',#4282,#1014);
#761=LINE('',#4283,#1015);
#762=LINE('',#4285,#1016);
#763=LINE('',#4286,#1017);
#991=VECTOR('',#3480,10.);
#992=VECTOR('',#3481,10.);
#993=VECTOR('',#3482,10.);
#994=VECTOR('',#3483,10.);
#995=VECTOR('',#3486,10.);
#996=VECTOR('',#3487,10.);
#997=VECTOR('',#3488,10.);
#998=VECTOR('',#3491,10.);
#999=VECTOR('',#3492,10.);
#1000=VECTOR('',#3493,10.);
#1001=VECTOR('',#3496,10.);
#1002=VECTOR('',#3497,10.);
#1003=VECTOR('',#3498,10.);
#1004=VECTOR('',#3501,10.);
#1005=VECTOR('',#3502,10.);
#1006=VECTOR('',#3503,10.);
#1007=VECTOR('',#3506,10.);
#1008=VECTOR('',#3507,10.);
#1009=VECTOR('',#3508,10.);
#1010=VECTOR('',#3511,10.);
#1011=VECTOR('',#3512,10.);
#1012=VECTOR('',#3513,10.);
#1013=VECTOR('',#3516,10.);
#1014=VECTOR('',#3517,10.);
#1015=VECTOR('',#3518,10.);
#1016=VECTOR('',#3521,10.);
#1017=VECTOR('',#3522,10.);
#1305=VERTEX_POINT('',#4234);
#1306=VERTEX_POINT('',#4235);
#1307=VERTEX_POINT('',#4237);
#1308=VERTEX_POINT('',#4239);
#1309=VERTEX_POINT('',#4243);
#1310=VERTEX_POINT('',#4245);
#1311=VERTEX_POINT('',#4249);
#1312=VERTEX_POINT('',#4251);
#1313=VERTEX_POINT('',#4255);
#1314=VERTEX_POINT('',#4257);
#1315=VERTEX_POINT('',#4261);
#1316=VERTEX_POINT('',#4263);
#1317=VERTEX_POINT('',#4267);
#1318=VERTEX_POINT('',#4269);
#1319=VERTEX_POINT('',#4273);
#1320=VERTEX_POINT('',#4275);
#1321=VERTEX_POINT('',#4279);
#1322=VERTEX_POINT('',#4281);
#1587=EDGE_CURVE('',#1305,#1306,#737,.T.);
#1588=EDGE_CURVE('',#1305,#1307,#738,.T.);
#1589=EDGE_CURVE('',#1308,#1307,#739,.T.);
#1590=EDGE_CURVE('',#1306,#1308,#740,.T.);
#1591=EDGE_CURVE('',#1307,#1309,#741,.T.);
#1592=EDGE_CURVE('',#1309,#1310,#742,.T.);
#1593=EDGE_CURVE('',#1310,#1308,#743,.T.);
#1594=EDGE_CURVE('',#1306,#1311,#744,.T.);
#1595=EDGE_CURVE('',#1311,#1312,#745,.T.);
#1596=EDGE_CURVE('',#1305,#1312,#746,.T.);
#1597=EDGE_CURVE('',#1311,#1313,#747,.T.);
#1598=EDGE_CURVE('',#1314,#1313,#748,.T.);
#1599=EDGE_CURVE('',#1312,#1314,#749,.T.);
#1600=EDGE_CURVE('',#1313,#1315,#750,.T.);
#1601=EDGE_CURVE('',#1315,#1316,#751,.T.);
#1602=EDGE_CURVE('',#1316,#1314,#752,.T.);
#1603=EDGE_CURVE('',#1317,#1310,#753,.T.);
#1604=EDGE_CURVE('',#1318,#1309,#754,.T.);
#1605=EDGE_CURVE('',#1317,#1318,#755,.T.);
#1606=EDGE_CURVE('',#1319,#1317,#756,.T.);
#1607=EDGE_CURVE('',#1320,#1318,#757,.T.);
#1608=EDGE_CURVE('',#1319,#1320,#758,.T.);
#1609=EDGE_CURVE('',#1321,#1319,#759,.T.);
#1610=EDGE_CURVE('',#1322,#1320,#760,.T.);
#1611=EDGE_CURVE('',#1321,#1322,#761,.T.);
#1612=EDGE_CURVE('',#1315,#1321,#762,.T.);
#1613=EDGE_CURVE('',#1322,#1316,#763,.T.);
#2093=ORIENTED_EDGE('',*,*,#1587,.F.);
#2094=ORIENTED_EDGE('',*,*,#1588,.T.);
#2095=ORIENTED_EDGE('',*,*,#1589,.F.);
#2096=ORIENTED_EDGE('',*,*,#1590,.F.);
#2097=ORIENTED_EDGE('',*,*,#1589,.T.);
#2098=ORIENTED_EDGE('',*,*,#1591,.T.);
#2099=ORIENTED_EDGE('',*,*,#1592,.T.);
#2100=ORIENTED_EDGE('',*,*,#1593,.T.);
#2101=ORIENTED_EDGE('',*,*,#1587,.T.);
#2102=ORIENTED_EDGE('',*,*,#1594,.T.);
#2103=ORIENTED_EDGE('',*,*,#1595,.T.);
#2104=ORIENTED_EDGE('',*,*,#1596,.F.);
#2105=ORIENTED_EDGE('',*,*,#1595,.F.);
#2106=ORIENTED_EDGE('',*,*,#1597,.T.);
#2107=ORIENTED_EDGE('',*,*,#1598,.F.);
#2108=ORIENTED_EDGE('',*,*,#1599,.F.);
#2109=ORIENTED_EDGE('',*,*,#1598,.T.);
#2110=ORIENTED_EDGE('',*,*,#1600,.T.);
#2111=ORIENTED_EDGE('',*,*,#1601,.T.);
#2112=ORIENTED_EDGE('',*,*,#1602,.T.);
#2113=ORIENTED_EDGE('',*,*,#1603,.T.);
#2114=ORIENTED_EDGE('',*,*,#1592,.F.);
#2115=ORIENTED_EDGE('',*,*,#1604,.F.);
#2116=ORIENTED_EDGE('',*,*,#1605,.F.);
#2117=ORIENTED_EDGE('',*,*,#1606,.T.);
#2118=ORIENTED_EDGE('',*,*,#1605,.T.);
#2119=ORIENTED_EDGE('',*,*,#1607,.F.);
#2120=ORIENTED_EDGE('',*,*,#1608,.F.);
#2121=ORIENTED_EDGE('',*,*,#1609,.T.);
#2122=ORIENTED_EDGE('',*,*,#1608,.T.);
#2123=ORIENTED_EDGE('',*,*,#1610,.F.);
#2124=ORIENTED_EDGE('',*,*,#1611,.F.);
#2125=ORIENTED_EDGE('',*,*,#1612,.T.);
#2126=ORIENTED_EDGE('',*,*,#1611,.T.);
#2127=ORIENTED_EDGE('',*,*,#1613,.T.);
#2128=ORIENTED_EDGE('',*,*,#1601,.F.);
#2129=ORIENTED_EDGE('',*,*,#1613,.F.);
#2130=ORIENTED_EDGE('',*,*,#1610,.T.);
#2131=ORIENTED_EDGE('',*,*,#1607,.T.);
#2132=ORIENTED_EDGE('',*,*,#1604,.T.);
#2133=ORIENTED_EDGE('',*,*,#1591,.F.);
#2134=ORIENTED_EDGE('',*,*,#1588,.F.);
#2135=ORIENTED_EDGE('',*,*,#1596,.T.);
#2136=ORIENTED_EDGE('',*,*,#1599,.T.);
#2137=ORIENTED_EDGE('',*,*,#1602,.F.);
#2138=ORIENTED_EDGE('',*,*,#1612,.F.);
#2139=ORIENTED_EDGE('',*,*,#1600,.F.);
#2140=ORIENTED_EDGE('',*,*,#1597,.F.);
#2141=ORIENTED_EDGE('',*,*,#1594,.F.);
#2142=ORIENTED_EDGE('',*,*,#1590,.T.);
#2143=ORIENTED_EDGE('',*,*,#1593,.F.);
#2144=ORIENTED_EDGE('',*,*,#1603,.F.);
#2145=ORIENTED_EDGE('',*,*,#1606,.F.);
#2146=ORIENTED_EDGE('',*,*,#1609,.F.);
#2609=ADVANCED_FACE('',(#351),#215,.T.);
#2610=ADVANCED_FACE('',(#352),#216,.T.);
#2611=ADVANCED_FACE('',(#353),#217,.T.);
#2612=ADVANCED_FACE('',(#354),#218,.T.);
#2613=ADVANCED_FACE('',(#355),#219,.T.);
#2614=ADVANCED_FACE('',(#356),#220,.T.);
#2615=ADVANCED_FACE('',(#357),#221,.T.);
#2616=ADVANCED_FACE('',(#358),#222,.T.);
#2617=ADVANCED_FACE('',(#359),#223,.T.);
#2618=ADVANCED_FACE('',(#360),#224,.T.);
#2619=ADVANCED_FACE('',(#361),#225,.F.);
#2693=CLOSED_SHELL('',(#2609,#2610,#2611,#2612,#2613,#2614,#2615,#2616,
#2617,#2618,#2619));
#2958=AXIS2_PLACEMENT_3D('',#4232,#3476,#3477);
#2959=AXIS2_PLACEMENT_3D('',#4233,#3478,#3479);
#2960=AXIS2_PLACEMENT_3D('',#4242,#3484,#3485);
#2961=AXIS2_PLACEMENT_3D('',#4248,#3489,#3490);
#2962=AXIS2_PLACEMENT_3D('',#4254,#3494,#3495);
#2963=AXIS2_PLACEMENT_3D('',#4260,#3499,#3500);
#2964=AXIS2_PLACEMENT_3D('',#4266,#3504,#3505);
#2965=AXIS2_PLACEMENT_3D('',#4272,#3509,#3510);
#2966=AXIS2_PLACEMENT_3D('',#4278,#3514,#3515);
#2967=AXIS2_PLACEMENT_3D('',#4284,#3519,#3520);
#2968=AXIS2_PLACEMENT_3D('',#4287,#3523,#3524);
#2969=AXIS2_PLACEMENT_3D('',#4288,#3525,#3526);
#3476=DIRECTION('axis',(0.,0.,1.));
#3477=DIRECTION('refdir',(1.,0.,0.));
#3478=DIRECTION('center_axis',(0.,1.,0.));
#3479=DIRECTION('ref_axis',(-1.,0.,0.));
#3480=DIRECTION('',(1.,0.,0.));
#3481=DIRECTION('',(0.,0.,1.));
#3482=DIRECTION('',(-1.,0.,0.));
#3483=DIRECTION('',(0.,0.,1.));
#3484=DIRECTION('center_axis',(0.,0.,1.));
#3485=DIRECTION('ref_axis',(1.,0.,0.));
#3486=DIRECTION('',(0.,-1.,0.));
#3487=DIRECTION('',(1.,0.,0.));
#3488=DIRECTION('',(0.,1.,0.));
#3489=DIRECTION('center_axis',(0.,0.,1.));
#3490=DIRECTION('ref_axis',(0.,1.,0.));
#3491=DIRECTION('',(0.,1.,0.));
#3492=DIRECTION('',(-1.,0.,0.));
#3493=DIRECTION('',(0.,1.,0.));
#3494=DIRECTION('center_axis',(0.,-1.,0.));
#3495=DIRECTION('ref_axis',(1.,0.,0.));
#3496=DIRECTION('',(0.,0.,1.));
#3497=DIRECTION('',(1.,0.,0.));
#3498=DIRECTION('',(0.,0.,1.));
#3499=DIRECTION('center_axis',(0.,0.,1.));
#3500=DIRECTION('ref_axis',(1.,0.,0.));
#3501=DIRECTION('',(0.,1.,0.));
#3502=DIRECTION('',(-1.,0.,0.));
#3503=DIRECTION('',(0.,-1.,0.));
#3504=DIRECTION('center_axis',(0.,-1.,0.));
#3505=DIRECTION('ref_axis',(0.,0.,1.));
#3506=DIRECTION('',(0.,0.,1.));
#3507=DIRECTION('',(0.,0.,1.));
#3508=DIRECTION('',(-1.,0.,0.));
#3509=DIRECTION('center_axis',(0.,-0.707106781186547,-0.707106781186548));
#3510=DIRECTION('ref_axis',(0.,-0.707106781186548,0.707106781186547));
#3511=DIRECTION('',(0.,-0.707106781186548,0.707106781186547));
#3512=DIRECTION('',(0.,-0.707106781186548,0.707106781186547));
#3513=DIRECTION('',(-1.,0.,0.));
#3514=DIRECTION('center_axis',(0.,0.,-1.));
#3515=DIRECTION('ref_axis',(0.,-1.,0.));
#3516=DIRECTION('',(0.,-1.,0.));
#3517=DIRECTION('',(0.,-1.,0.));
#3518=DIRECTION('',(-1.,0.,0.));
#3519=DIRECTION('center_axis',(0.,1.,0.));
#3520=DIRECTION('ref_axis',(0.,0.,-1.));
#3521=DIRECTION('',(0.,0.,-1.));
#3522=DIRECTION('',(0.,0.,1.));
#3523=DIRECTION('center_axis',(-1.,0.,0.));
#3524=DIRECTION('ref_axis',(0.,0.,1.));
#3525=DIRECTION('center_axis',(-1.,0.,0.));
#3526=DIRECTION('ref_axis',(0.,-1.,0.));
#4232=CARTESIAN_POINT('',(0.,0.,0.));
#4233=CARTESIAN_POINT('Origin',(70.,-60.0000000000105,-5.99999999999788));
#4234=CARTESIAN_POINT('',(-90.,-60.0000000000105,-5.99999999999788));
#4235=CARTESIAN_POINT('',(70.,-60.0000000000105,-5.99999999999788));
#4236=CARTESIAN_POINT('',(70.,-60.0000000000105,-5.99999999999788));
#4237=CARTESIAN_POINT('',(-90.,-60.0000000000105,4.00000000000212));
#4238=CARTESIAN_POINT('',(-90.,-60.0000000000105,-5.99999999999788));
#4239=CARTESIAN_POINT('',(70.,-60.0000000000105,4.00000000000212));
#4240=CARTESIAN_POINT('',(70.,-60.0000000000105,4.00000000000212));
#4241=CARTESIAN_POINT('',(70.,-60.0000000000105,-5.99999999999788));
#4242=CARTESIAN_POINT('Origin',(-10.,-75.0000000000105,4.00000000000212));
#4243=CARTESIAN_POINT('',(-90.,-90.0000000000105,4.00000000000212));
#4244=CARTESIAN_POINT('',(-90.,-60.0000000000105,4.00000000000212));
#4245=CARTESIAN_POINT('',(70.,-90.0000000000105,4.00000000000212));
#4246=CARTESIAN_POINT('',(-90.,-90.0000000000105,4.00000000000212));
#4247=CARTESIAN_POINT('',(70.,-90.0000000000105,4.00000000000212));
#4248=CARTESIAN_POINT('Origin',(70.,-90.0000000000105,-5.99999999999788));
#4249=CARTESIAN_POINT('',(70.,-1.05160324892495E-11,-5.99999999999788));
#4250=CARTESIAN_POINT('',(70.,-90.0000000000105,-5.99999999999788));
#4251=CARTESIAN_POINT('',(-90.,-1.05160324892495E-11,-5.99999999999788));
#4252=CARTESIAN_POINT('',(-10.,-1.05160324892495E-11,-5.99999999999788));
#4253=CARTESIAN_POINT('',(-90.,-90.0000000000105,-5.99999999999788));
#4254=CARTESIAN_POINT('Origin',(-90.,-1.05160324892495E-11,-5.99999999999788));
#4255=CARTESIAN_POINT('',(70.,-1.05160324892495E-11,4.00000000000212));
#4256=CARTESIAN_POINT('',(70.,-1.05160324892495E-11,-5.99999999999788));
#4257=CARTESIAN_POINT('',(-90.,-1.05160324892495E-11,4.00000000000212));
#4258=CARTESIAN_POINT('',(70.,-1.05160324892495E-11,4.00000000000212));
#4259=CARTESIAN_POINT('',(-90.,-1.05160324892495E-11,-5.99999999999788));
#4260=CARTESIAN_POINT('Origin',(-10.,14.9999999999895,4.00000000000212));
#4261=CARTESIAN_POINT('',(70.,29.9999999999895,4.00000000000212));
#4262=CARTESIAN_POINT('',(70.,29.9999999999895,4.00000000000212));
#4263=CARTESIAN_POINT('',(-90.,29.9999999999895,4.00000000000212));
#4264=CARTESIAN_POINT('',(-90.,29.9999999999895,4.00000000000212));
#4265=CARTESIAN_POINT('',(-90.,-1.05160324892495E-11,4.00000000000212));
#4266=CARTESIAN_POINT('Origin',(70.,-90.0000000000105,-14.9999999999979));
#4267=CARTESIAN_POINT('',(70.,-90.0000000000105,-14.9999999999979));
#4268=CARTESIAN_POINT('',(70.,-90.0000000000105,-19.9999999999979));
#4269=CARTESIAN_POINT('',(-90.,-90.0000000000105,-14.9999999999979));
#4270=CARTESIAN_POINT('',(-90.,-90.0000000000105,-19.9999999999979));
#4271=CARTESIAN_POINT('',(70.,-90.0000000000105,-14.9999999999979));
#4272=CARTESIAN_POINT('Origin',(70.,-85.0000000000105,-19.9999999999979));
#4273=CARTESIAN_POINT('',(70.,-85.0000000000105,-19.9999999999979));
#4274=CARTESIAN_POINT('',(70.,-85.0000000000105,-19.9999999999979));
#4275=CARTESIAN_POINT('',(-90.,-85.0000000000105,-19.9999999999979));
#4276=CARTESIAN_POINT('',(-90.,-85.0000000000105,-19.9999999999979));
#4277=CARTESIAN_POINT('',(70.,-85.0000000000105,-19.9999999999979));
#4278=CARTESIAN_POINT('Origin',(70.,29.9999999999895,-19.9999999999979));
#4279=CARTESIAN_POINT('',(70.,29.9999999999895,-19.9999999999979));
#4280=CARTESIAN_POINT('',(70.,29.9999999999895,-19.9999999999979));
#4281=CARTESIAN_POINT('',(-90.,29.9999999999895,-19.9999999999979));
#4282=CARTESIAN_POINT('',(-90.,29.9999999999895,-19.9999999999979));
#4283=CARTESIAN_POINT('',(70.,29.9999999999895,-19.9999999999979));
#4284=CARTESIAN_POINT('Origin',(70.,29.9999999999895,-5.99999999999788));
#4285=CARTESIAN_POINT('',(70.,29.9999999999895,-5.99999999999788));
#4286=CARTESIAN_POINT('',(-90.,29.9999999999895,-5.99999999999788));
#4287=CARTESIAN_POINT('Origin',(-90.,-30.0000000000105,-12.9999999999979));
#4288=CARTESIAN_POINT('Origin',(70.,-30.0000000000105,-12.9999999999979));
#4815=UNCERTAINTY_MEASURE_WITH_UNIT(LENGTH_MEASURE(0.01),#4834,
'DISTANCE_ACCURACY_VALUE',
'Maximum model space distance between geometric entities at asserted c
onnectivities');
#4820=UNCERTAINTY_MEASURE_WITH_UNIT(LENGTH_MEASURE(0.01),#4834,
'DISTANCE_ACCURACY_VALUE',
'Maximum model space distance between geometric entities at asserted c
onnectivities');
#4828=(
GEOMETRIC_REPRESENTATION_CONTEXT(3)
GLOBAL_UNCERTAINTY_ASSIGNED_CONTEXT((#4815))
GLOBAL_UNIT_ASSIGNED_CONTEXT((#4834,#4836,#4837))
REPRESENTATION_CONTEXT('','3D')
);
#4833=(
GEOMETRIC_REPRESENTATION_CONTEXT(3)
GLOBAL_UNCERTAINTY_ASSIGNED_CONTEXT((#4820))
GLOBAL_UNIT_ASSIGNED_CONTEXT((#4834,#4836,#4837))
REPRESENTATION_CONTEXT('','3D')
);
#4834=(
LENGTH_UNIT()
NAMED_UNIT(*)
SI_UNIT(.MILLI.,.METRE.)
);
#4836=(
NAMED_UNIT(*)
PLANE_ANGLE_UNIT()
SI_UNIT($,.RADIAN.)
);
#4837=(
NAMED_UNIT(*)
SI_UNIT($,.STERADIAN.)
SOLID_ANGLE_UNIT()
);
#4845=SHAPE_DEFINITION_REPRESENTATION(#4857,#4880);
#4857=PRODUCT_DEFINITION_SHAPE('',$,#4893);
#4880=SHAPE_REPRESENTATION('',(#2958),#4828);
#4885=PRODUCT_DEFINITION_CONTEXT('part definition',#4923,'design');
#4893=PRODUCT_DEFINITION('Base','Base',#4905,#4885);
#4905=PRODUCT_DEFINITION_FORMATION('',$,#4932);
#4923=APPLICATION_CONTEXT(
'Core Data for Automotive Mechanical Design Process');
#4924=PRODUCT_CONTEXT('part definition',#4923,'mechanical');
#4932=PRODUCT('Base','Base',$,(#4924));
#4965=COLOUR_RGB('Dark Blue',0.08,0.2,0.34);
#4966=FILL_AREA_STYLE_COLOUR('',#4965);
#4967=FILL_AREA_STYLE('',(#4966));
#4968=SURFACE_STYLE_FILL_AREA(#4967);
#4969=SURFACE_SIDE_STYLE('',(#4968));
#4970=SURFACE_STYLE_USAGE(.BOTH.,#4969);
#4971=PRESENTATION_STYLE_ASSIGNMENT((#4970));
ENDSEC;
END-ISO-10303-21;
